ISO-10303-21;
HEADER;
/* Generated by software containing ST-Developer
 * from STEP Tools, Inc. (www.steptools.com) 
 */

FILE_DESCRIPTION(
/* description */ ('Wall-mounted air drop station'),
/* implementation_level */ '2;1');

FILE_NAME(
/* name */ 'Hex Nut - M5.step',
/* time_stamp */ '2026-10-28T22:16:19-07:00',
/* author */ (''),
/* organization */ (''),
/* preprocessor_version */ 'ST-DEVELOPER v20.2',
/* originating_system */ 'Autodesk Translation Framework v15.17.0.0',
/* authorisation */ '');

FILE_SCHEMA (('AUTOMOTIVE_DESIGN { 1 0 10303 214 3 1 1 }'));
ENDSEC;

DATA;
#10=MECHANICAL_DESIGN_GEOMETRIC_PRESENTATION_REPRESENTATION('',(#359),#10517);
#233=(
BOUNDED_CURVE()
B_SPLINE_CURVE(2,(#9666,#9667,#9668),.UNSPECIFIED.,.F.,.F.)
B_SPLINE_CURVE_WITH_KNOTS((3,3),(0.140651836354967,0.670383167684795),
 .UNSPECIFIED.)
CURVE()
GEOMETRIC_REPRESENTATION_ITEM()
RATIONAL_B_SPLINE_CURVE((1.11602540378444,1.28867513459481,1.11602540378444))
REPRESENTATION_ITEM('')
);
#234=(
BOUNDED_CURVE()
B_SPLINE_CURVE(2,(#9670,#9671,#9672),.UNSPECIFIED.,.F.,.F.)
B_SPLINE_CURVE_WITH_KNOTS((3,3),(0.140651836354967,0.670383167684795),
 .UNSPECIFIED.)
CURVE()
GEOMETRIC_REPRESENTATION_ITEM()
RATIONAL_B_SPLINE_CURVE((1.11602540378444,1.28867513459481,1.11602540378444))
REPRESENTATION_ITEM('')
);
#235=(
BOUNDED_CURVE()
B_SPLINE_CURVE(2,(#9677,#9678,#9679),.UNSPECIFIED.,.F.,.F.)
B_SPLINE_CURVE_WITH_KNOTS((3,3),(0.140651836354967,0.670383167684795),
 .UNSPECIFIED.)
CURVE()
GEOMETRIC_REPRESENTATION_ITEM()
RATIONAL_B_SPLINE_CURVE((1.11602540378444,1.28867513459481,1.11602540378444))
REPRESENTATION_ITEM('')
);
#236=(
BOUNDED_CURVE()
B_SPLINE_CURVE(2,(#9681,#9682,#9683),.UNSPECIFIED.,.F.,.F.)
B_SPLINE_CURVE_WITH_KNOTS((3,3),(0.140651836354967,0.670383167684795),
 .UNSPECIFIED.)
CURVE()
GEOMETRIC_REPRESENTATION_ITEM()
RATIONAL_B_SPLINE_CURVE((1.11602540378444,1.28867513459481,1.11602540378444))
REPRESENTATION_ITEM('')
);
#237=(
BOUNDED_CURVE()
B_SPLINE_CURVE(2,(#9685,#9686,#9687),.UNSPECIFIED.,.F.,.F.)
B_SPLINE_CURVE_WITH_KNOTS((3,3),(0.140651836354967,0.670383167684795),
 .UNSPECIFIED.)
CURVE()
GEOMETRIC_REPRESENTATION_ITEM()
RATIONAL_B_SPLINE_CURVE((1.11602540378444,1.28867513459481,1.11602540378444))
REPRESENTATION_ITEM('')
);
#238=(
BOUNDED_CURVE()
B_SPLINE_CURVE(2,(#9688,#9689,#9690),.UNSPECIFIED.,.F.,.F.)
B_SPLINE_CURVE_WITH_KNOTS((3,3),(0.140651836354967,0.670383167684795),
 .UNSPECIFIED.)
CURVE()
GEOMETRIC_REPRESENTATION_ITEM()
RATIONAL_B_SPLINE_CURVE((1.11602540378444,1.28867513459481,1.11602540378444))
REPRESENTATION_ITEM('')
);
#239=(
BOUNDED_CURVE()
B_SPLINE_CURVE(2,(#9697,#9698,#9699),.UNSPECIFIED.,.F.,.F.)
B_SPLINE_CURVE_WITH_KNOTS((3,3),(0.140651836354967,0.670383167684795),
 .UNSPECIFIED.)
CURVE()
GEOMETRIC_REPRESENTATION_ITEM()
RATIONAL_B_SPLINE_CURVE((1.11602540378444,1.28867513459481,1.11602540378444))
REPRESENTATION_ITEM('')
);
#240=(
BOUNDED_CURVE()
B_SPLINE_CURVE(2,(#9701,#9702,#9703),.UNSPECIFIED.,.F.,.F.)
B_SPLINE_CURVE_WITH_KNOTS((3,3),(0.140651836354967,0.670383167684796),
 .UNSPECIFIED.)
CURVE()
GEOMETRIC_REPRESENTATION_ITEM()
RATIONAL_B_SPLINE_CURVE((1.11602540378444,1.28867513459481,1.11602540378444))
REPRESENTATION_ITEM('')
);
#241=(
BOUNDED_CURVE()
B_SPLINE_CURVE(2,(#9705,#9706,#9707),.UNSPECIFIED.,.F.,.F.)
B_SPLINE_CURVE_WITH_KNOTS((3,3),(0.140651836354967,0.670383167684795),
 .UNSPECIFIED.)
CURVE()
GEOMETRIC_REPRESENTATION_ITEM()
RATIONAL_B_SPLINE_CURVE((1.11602540378444,1.28867513459481,1.11602540378444))
REPRESENTATION_ITEM('')
);
#242=(
BOUNDED_CURVE()
B_SPLINE_CURVE(2,(#9709,#9710,#9711),.UNSPECIFIED.,.F.,.F.)
B_SPLINE_CURVE_WITH_KNOTS((3,3),(0.140651836354967,0.670383167684795),
 .UNSPECIFIED.)
CURVE()
GEOMETRIC_REPRESENTATION_ITEM()
RATIONAL_B_SPLINE_CURVE((1.11602540378444,1.28867513459482,1.11602540378444))
REPRESENTATION_ITEM('')
);
#243=(
BOUNDED_CURVE()
B_SPLINE_CURVE(2,(#9713,#9714,#9715),.UNSPECIFIED.,.F.,.F.)
B_SPLINE_CURVE_WITH_KNOTS((3,3),(0.140651836354967,0.670383167684795),
 .UNSPECIFIED.)
CURVE()
GEOMETRIC_REPRESENTATION_ITEM()
RATIONAL_B_SPLINE_CURVE((1.11602540378444,1.28867513459481,1.11602540378444))
REPRESENTATION_ITEM('')
);
#244=(
BOUNDED_CURVE()
B_SPLINE_CURVE(2,(#9716,#9717,#9718),.UNSPECIFIED.,.F.,.F.)
B_SPLINE_CURVE_WITH_KNOTS((3,3),(0.140651836354967,0.670383167684795),
 .UNSPECIFIED.)
CURVE()
GEOMETRIC_REPRESENTATION_ITEM()
RATIONAL_B_SPLINE_CURVE((1.11602540378444,1.28867513459481,1.11602540378444))
REPRESENTATION_ITEM('')
);
#271=CONICAL_SURFACE('',#6605,0.47094010767585,1.0471975511966);
#272=CONICAL_SURFACE('',#6607,0.47094010767585,1.0471975511966);
#301=SHAPE_REPRESENTATION_RELATIONSHIP('SRR','None',#10658,#330);
#330=ADVANCED_BREP_SHAPE_REPRESENTATION('',(#387),#10502);
#359=STYLED_ITEM('',(#10881),#387);
#387=MANIFOLD_SOLID_BREP('Body1',#5899);
#496=FACE_BOUND('',#1414,.T.);
#497=FACE_BOUND('',#1416,.T.);
#643=PLANE('',#6609);
#644=PLANE('',#6610);
#645=PLANE('',#6611);
#646=PLANE('',#6615);
#647=PLANE('',#6616);
#648=PLANE('',#6617);
#649=PLANE('',#6618);
#650=PLANE('',#6619);
#952=FACE_OUTER_BOUND('',#1404,.T.);
#953=FACE_OUTER_BOUND('',#1405,.T.);
#954=FACE_OUTER_BOUND('',#1406,.T.);
#955=FACE_OUTER_BOUND('',#1407,.T.);
#956=FACE_OUTER_BOUND('',#1408,.T.);
#957=FACE_OUTER_BOUND('',#1409,.T.);
#958=FACE_OUTER_BOUND('',#1410,.T.);
#959=FACE_OUTER_BOUND('',#1411,.T.);
#960=FACE_OUTER_BOUND('',#1412,.T.);
#961=FACE_OUTER_BOUND('',#1413,.T.);
#962=FACE_OUTER_BOUND('',#1415,.T.);
#1404=EDGE_LOOP('',(#4793,#4794,#4795,#4796,#4797,#4798,#4799,#4800,#4801));
#1405=EDGE_LOOP('',(#4802,#4803,#4804,#4805,#4806,#4807,#4808,#4809,#4810));
#1406=EDGE_LOOP('',(#4811,#4812,#4813,#4814));
#1407=EDGE_LOOP('',(#4815,#4816,#4817,#4818));
#1408=EDGE_LOOP('',(#4819,#4820,#4821,#4822));
#1409=EDGE_LOOP('',(#4823,#4824,#4825,#4826));
#1410=EDGE_LOOP('',(#4827,#4828,#4829,#4830));
#1411=EDGE_LOOP('',(#4831,#4832,#4833,#4834));
#1412=EDGE_LOOP('',(#4835,#4836,#4837,#4838));
#1413=EDGE_LOOP('',(#4839));
#1414=EDGE_LOOP('',(#4840));
#1415=EDGE_LOOP('',(#4841));
#1416=EDGE_LOOP('',(#4842));
#1847=LINE('',#9674,#2311);
#1848=LINE('',#9695,#2312);
#1849=LINE('',#9720,#2313);
#1850=LINE('',#9721,#2314);
#1851=LINE('',#9723,#2315);
#1852=LINE('',#9725,#2316);
#1853=LINE('',#9730,#2317);
#1854=LINE('',#9733,#2318);
#1855=LINE('',#9735,#2319);
#2311=VECTOR('',#7921,0.47094010767585);
#2312=VECTOR('',#7928,0.47094010767585);
#2313=VECTOR('',#7931,1.);
#2314=VECTOR('',#7932,1.);
#2315=VECTOR('',#7935,1.);
#2316=VECTOR('',#7938,1.);
#2317=VECTOR('',#7943,0.25);
#2318=VECTOR('',#7948,1.);
#2319=VECTOR('',#7951,1.);
#2675=CIRCLE('',#6606,0.38);
#2676=CIRCLE('',#6608,0.38);
#2677=CIRCLE('',#6613,0.2117);
#2678=CIRCLE('',#6614,0.2117);
#3037=VERTEX_POINT('',#9664);
#3038=VERTEX_POINT('',#9665);
#3039=VERTEX_POINT('',#9669);
#3040=VERTEX_POINT('',#9673);
#3041=VERTEX_POINT('',#9676);
#3042=VERTEX_POINT('',#9680);
#3043=VERTEX_POINT('',#9684);
#3044=VERTEX_POINT('',#9692);
#3045=VERTEX_POINT('',#9694);
#3046=VERTEX_POINT('',#9696);
#3047=VERTEX_POINT('',#9700);
#3048=VERTEX_POINT('',#9704);
#3049=VERTEX_POINT('',#9708);
#3050=VERTEX_POINT('',#9712);
#3051=VERTEX_POINT('',#9727);
#3052=VERTEX_POINT('',#9729);
#3654=EDGE_CURVE('',#3037,#3038,#233,.T.);
#3655=EDGE_CURVE('',#3039,#3037,#234,.T.);
#3656=EDGE_CURVE('',#3039,#3040,#1847,.T.);
#3657=EDGE_CURVE('',#3040,#3040,#2675,.T.);
#3658=EDGE_CURVE('',#3041,#3039,#235,.T.);
#3659=EDGE_CURVE('',#3042,#3041,#236,.T.);
#3660=EDGE_CURVE('',#3043,#3042,#237,.T.);
#3661=EDGE_CURVE('',#3038,#3043,#238,.T.);
#3662=EDGE_CURVE('',#3044,#3044,#2676,.T.);
#3663=EDGE_CURVE('',#3044,#3045,#1848,.T.);
#3664=EDGE_CURVE('',#3046,#3045,#239,.T.);
#3665=EDGE_CURVE('',#3047,#3046,#240,.T.);
#3666=EDGE_CURVE('',#3048,#3047,#241,.T.);
#3667=EDGE_CURVE('',#3049,#3048,#242,.T.);
#3668=EDGE_CURVE('',#3050,#3049,#243,.T.);
#3669=EDGE_CURVE('',#3045,#3050,#244,.T.);
#3670=EDGE_CURVE('',#3041,#3050,#1849,.T.);
#3671=EDGE_CURVE('',#3042,#3049,#1850,.T.);
#3672=EDGE_CURVE('',#3039,#3045,#1851,.T.);
#3673=EDGE_CURVE('',#3037,#3046,#1852,.T.);
#3674=EDGE_CURVE('',#3051,#3051,#2677,.F.);
#3675=EDGE_CURVE('',#3051,#3052,#1853,.T.);
#3676=EDGE_CURVE('',#3052,#3052,#2678,.F.);
#3677=EDGE_CURVE('',#3038,#3047,#1854,.T.);
#3678=EDGE_CURVE('',#3043,#3048,#1855,.T.);
#4793=ORIENTED_EDGE('',*,*,#3654,.F.);
#4794=ORIENTED_EDGE('',*,*,#3655,.F.);
#4795=ORIENTED_EDGE('',*,*,#3656,.T.);
#4796=ORIENTED_EDGE('',*,*,#3657,.F.);
#4797=ORIENTED_EDGE('',*,*,#3656,.F.);
#4798=ORIENTED_EDGE('',*,*,#3658,.F.);
#4799=ORIENTED_EDGE('',*,*,#3659,.F.);
#4800=ORIENTED_EDGE('',*,*,#3660,.F.);
#4801=ORIENTED_EDGE('',*,*,#3661,.F.);
#4802=ORIENTED_EDGE('',*,*,#3662,.F.);
#4803=ORIENTED_EDGE('',*,*,#3663,.T.);
#4804=ORIENTED_EDGE('',*,*,#3664,.F.);
#4805=ORIENTED_EDGE('',*,*,#3665,.F.);
#4806=ORIENTED_EDGE('',*,*,#3666,.F.);
#4807=ORIENTED_EDGE('',*,*,#3667,.F.);
#4808=ORIENTED_EDGE('',*,*,#3668,.F.);
#4809=ORIENTED_EDGE('',*,*,#3669,.F.);
#4810=ORIENTED_EDGE('',*,*,#3663,.F.);
#4811=ORIENTED_EDGE('',*,*,#3659,.T.);
#4812=ORIENTED_EDGE('',*,*,#3670,.T.);
#4813=ORIENTED_EDGE('',*,*,#3668,.T.);
#4814=ORIENTED_EDGE('',*,*,#3671,.F.);
#4815=ORIENTED_EDGE('',*,*,#3658,.T.);
#4816=ORIENTED_EDGE('',*,*,#3672,.T.);
#4817=ORIENTED_EDGE('',*,*,#3669,.T.);
#4818=ORIENTED_EDGE('',*,*,#3670,.F.);
#4819=ORIENTED_EDGE('',*,*,#3655,.T.);
#4820=ORIENTED_EDGE('',*,*,#3673,.T.);
#4821=ORIENTED_EDGE('',*,*,#3664,.T.);
#4822=ORIENTED_EDGE('',*,*,#3672,.F.);
#4823=ORIENTED_EDGE('',*,*,#3674,.F.);
#4824=ORIENTED_EDGE('',*,*,#3675,.T.);
#4825=ORIENTED_EDGE('',*,*,#3676,.T.);
#4826=ORIENTED_EDGE('',*,*,#3675,.F.);
#4827=ORIENTED_EDGE('',*,*,#3654,.T.);
#4828=ORIENTED_EDGE('',*,*,#3677,.T.);
#4829=ORIENTED_EDGE('',*,*,#3665,.T.);
#4830=ORIENTED_EDGE('',*,*,#3673,.F.);
#4831=ORIENTED_EDGE('',*,*,#3660,.T.);
#4832=ORIENTED_EDGE('',*,*,#3671,.T.);
#4833=ORIENTED_EDGE('',*,*,#3667,.T.);
#4834=ORIENTED_EDGE('',*,*,#3678,.F.);
#4835=ORIENTED_EDGE('',*,*,#3661,.T.);
#4836=ORIENTED_EDGE('',*,*,#3678,.T.);
#4837=ORIENTED_EDGE('',*,*,#3666,.T.);
#4838=ORIENTED_EDGE('',*,*,#3677,.F.);
#4839=ORIENTED_EDGE('',*,*,#3662,.T.);
#4840=ORIENTED_EDGE('',*,*,#3674,.T.);
#4841=ORIENTED_EDGE('',*,*,#3657,.T.);
#4842=ORIENTED_EDGE('',*,*,#3676,.F.);
#5500=CYLINDRICAL_SURFACE('',#6612,0.2117);
#5725=ADVANCED_FACE('',(#952),#271,.T.);
#5726=ADVANCED_FACE('',(#953),#272,.T.);
#5727=ADVANCED_FACE('',(#954),#643,.T.);
#5728=ADVANCED_FACE('',(#955),#644,.T.);
#5729=ADVANCED_FACE('',(#956),#645,.T.);
#5730=ADVANCED_FACE('',(#957),#5500,.F.);
#5731=ADVANCED_FACE('',(#958),#646,.T.);
#5732=ADVANCED_FACE('',(#959),#647,.T.);
#5733=ADVANCED_FACE('',(#960),#648,.T.);
#5734=ADVANCED_FACE('',(#961,#496),#649,.T.);
#5735=ADVANCED_FACE('',(#962,#497),#650,.F.);
#5899=CLOSED_SHELL('',(#5725,#5726,#5727,#5728,#5729,#5730,#5731,#5732,
#5733,#5734,#5735));
#6604=AXIS2_PLACEMENT_3D('',#9662,#7917,#7918);
#6605=AXIS2_PLACEMENT_3D('',#9663,#7919,#7920);
#6606=AXIS2_PLACEMENT_3D('',#9675,#7922,#7923);
#6607=AXIS2_PLACEMENT_3D('',#9691,#7924,#7925);
#6608=AXIS2_PLACEMENT_3D('',#9693,#7926,#7927);
#6609=AXIS2_PLACEMENT_3D('',#9719,#7929,#7930);
#6610=AXIS2_PLACEMENT_3D('',#9722,#7933,#7934);
#6611=AXIS2_PLACEMENT_3D('',#9724,#7936,#7937);
#6612=AXIS2_PLACEMENT_3D('',#9726,#7939,#7940);
#6613=AXIS2_PLACEMENT_3D('',#9728,#7941,#7942);
#6614=AXIS2_PLACEMENT_3D('',#9731,#7944,#7945);
#6615=AXIS2_PLACEMENT_3D('',#9732,#7946,#7947);
#6616=AXIS2_PLACEMENT_3D('',#9734,#7949,#7950);
#6617=AXIS2_PLACEMENT_3D('',#9736,#7952,#7953);
#6618=AXIS2_PLACEMENT_3D('',#9737,#7954,#7955);
#6619=AXIS2_PLACEMENT_3D('',#9738,#7956,#7957);
#7917=DIRECTION('axis',(0.,0.,1.));
#7918=DIRECTION('refdir',(1.,0.,0.));
#7919=DIRECTION('center_axis',(0.,1.,0.));
#7920=DIRECTION('ref_axis',(1.,0.,0.));
#7921=DIRECTION('',(0.866025403784439,-0.5,1.06057523872491E-16));
#7922=DIRECTION('center_axis',(0.,-1.,0.));
#7923=DIRECTION('ref_axis',(1.,0.,0.));
#7924=DIRECTION('center_axis',(0.,-1.,0.));
#7925=DIRECTION('ref_axis',(1.,0.,0.));
#7926=DIRECTION('center_axis',(0.,1.,0.));
#7927=DIRECTION('ref_axis',(1.,0.,0.));
#7928=DIRECTION('',(-0.866025403784439,-0.5,-1.06057523872491E-16));
#7929=DIRECTION('center_axis',(1.20185167898973E-16,0.,-1.));
#7930=DIRECTION('ref_axis',(-1.,0.,-1.20185167898973E-16));
#7931=DIRECTION('',(0.,1.,0.));
#7932=DIRECTION('',(0.,1.,0.));
#7933=DIRECTION('center_axis',(-0.866025403784439,0.,-0.5));
#7934=DIRECTION('ref_axis',(-0.5,0.,0.866025403784439));
#7935=DIRECTION('',(0.,1.,0.));
#7936=DIRECTION('center_axis',(-0.866025403784439,0.,0.5));
#7937=DIRECTION('ref_axis',(0.5,0.,0.866025403784439));
#7938=DIRECTION('',(0.,1.,0.));
#7939=DIRECTION('center_axis',(0.,1.,0.));
#7940=DIRECTION('ref_axis',(1.,0.,0.));
#7941=DIRECTION('center_axis',(0.,1.,0.));
#7942=DIRECTION('ref_axis',(1.,0.,0.));
#7943=DIRECTION('',(0.,-1.,0.));
#7944=DIRECTION('center_axis',(0.,1.,0.));
#7945=DIRECTION('ref_axis',(1.,0.,0.));
#7946=DIRECTION('center_axis',(-2.40370335797945E-16,0.,1.));
#7947=DIRECTION('ref_axis',(1.,0.,2.40370335797945E-16));
#7948=DIRECTION('',(0.,1.,0.));
#7949=DIRECTION('center_axis',(0.866025403784439,0.,-0.5));
#7950=DIRECTION('ref_axis',(-0.5,0.,-0.866025403784439));
#7951=DIRECTION('',(0.,1.,0.));
#7952=DIRECTION('center_axis',(0.866025403784439,0.,0.5));
#7953=DIRECTION('ref_axis',(0.5,0.,-0.866025403784439));
#7954=DIRECTION('center_axis',(0.,1.,0.));
#7955=DIRECTION('ref_axis',(1.,0.,0.));
#7956=DIRECTION('center_axis',(0.,1.,0.));
#7957=DIRECTION('ref_axis',(1.,0.,0.));
#9662=CARTESIAN_POINT('',(0.,0.,0.));
#9663=CARTESIAN_POINT('Origin',(0.,0.0525042956467857,0.));
#9664=CARTESIAN_POINT('',(-0.230940107675851,0.0472735643746089,0.4));
#9665=CARTESIAN_POINT('',(0.23094010767585,0.0472735643746089,0.4));
#9666=CARTESIAN_POINT('Ctrl Pts',(-0.230940107675851,0.0472735643746089,
0.4));
#9667=CARTESIAN_POINT('Ctrl Pts',(1.11022302462516E-16,-0.0193931022920578,
0.4));
#9668=CARTESIAN_POINT('Ctrl Pts',(0.23094010767585,0.0472735643746089,0.4));
#9669=CARTESIAN_POINT('',(-0.461880215351701,0.0472735643746089,-5.6564012731995E-17));
#9670=CARTESIAN_POINT('Ctrl Pts',(-0.461880215351701,0.0472735643746089,
-5.6564012731995E-17));
#9671=CARTESIAN_POINT('Ctrl Pts',(-0.346410161513776,-0.0193931022920579,
0.2));
#9672=CARTESIAN_POINT('Ctrl Pts',(-0.230940107675851,0.0472735643746089,
0.4));
#9673=CARTESIAN_POINT('',(-0.38,-2.08166817117217E-17,-4.65365783675994E-17));
#9674=CARTESIAN_POINT('',(-0.47094010767585,0.0525042956467857,-5.7673529545534E-17));
#9675=CARTESIAN_POINT('Origin',(0.,0.,0.));
#9676=CARTESIAN_POINT('',(-0.23094010767585,0.0472735643746089,-0.4));
#9677=CARTESIAN_POINT('Ctrl Pts',(-0.23094010767585,0.0472735643746089,
-0.4));
#9678=CARTESIAN_POINT('Ctrl Pts',(-0.346410161513775,-0.0193931022920578,
-0.2));
#9679=CARTESIAN_POINT('Ctrl Pts',(-0.461880215351701,0.0472735643746089,
-5.6564012731995E-17));
#9680=CARTESIAN_POINT('',(0.23094010767585,0.0472735643746089,-0.4));
#9681=CARTESIAN_POINT('Ctrl Pts',(0.23094010767585,0.0472735643746089,-0.4));
#9682=CARTESIAN_POINT('Ctrl Pts',(0.,-0.0193931022920578,-0.4));
#9683=CARTESIAN_POINT('Ctrl Pts',(-0.23094010767585,0.0472735643746089,
-0.4));
#9684=CARTESIAN_POINT('',(0.461880215351701,0.0472735643746089,0.));
#9685=CARTESIAN_POINT('Ctrl Pts',(0.461880215351701,0.0472735643746089,
0.));
#9686=CARTESIAN_POINT('Ctrl Pts',(0.346410161513776,-0.019393102292058,
-0.2));
#9687=CARTESIAN_POINT('Ctrl Pts',(0.23094010767585,0.0472735643746089,-0.4));
#9688=CARTESIAN_POINT('Ctrl Pts',(0.23094010767585,0.0472735643746089,0.4));
#9689=CARTESIAN_POINT('Ctrl Pts',(0.346410161513776,-0.0193931022920577,
0.2));
#9690=CARTESIAN_POINT('Ctrl Pts',(0.461880215351701,0.0472735643746089,
0.));
#9691=CARTESIAN_POINT('Origin',(0.,0.417495704353214,0.));
#9692=CARTESIAN_POINT('',(-0.38,0.47,-4.65365783675994E-17));
#9693=CARTESIAN_POINT('Origin',(0.,0.47,0.));
#9694=CARTESIAN_POINT('',(-0.461880215351701,0.422726435625391,-5.6564012731995E-17));
#9695=CARTESIAN_POINT('',(-0.47094010767585,0.417495704353214,-5.7673529545534E-17));
#9696=CARTESIAN_POINT('',(-0.230940107675851,0.422726435625391,0.4));
#9697=CARTESIAN_POINT('Ctrl Pts',(-0.230940107675851,0.422726435625391,
0.4));
#9698=CARTESIAN_POINT('Ctrl Pts',(-0.346410161513776,0.489393102292058,
0.2));
#9699=CARTESIAN_POINT('Ctrl Pts',(-0.461880215351701,0.422726435625391,
-5.6564012731995E-17));
#9700=CARTESIAN_POINT('',(0.23094010767585,0.422726435625391,0.4));
#9701=CARTESIAN_POINT('Ctrl Pts',(0.23094010767585,0.422726435625391,0.4));
#9702=CARTESIAN_POINT('Ctrl Pts',(8.32667268468867E-17,0.489393102292058,
0.4));
#9703=CARTESIAN_POINT('Ctrl Pts',(-0.230940107675851,0.422726435625391,
0.4));
#9704=CARTESIAN_POINT('',(0.461880215351701,0.422726435625391,0.));
#9705=CARTESIAN_POINT('Ctrl Pts',(0.461880215351701,0.422726435625391,0.));
#9706=CARTESIAN_POINT('Ctrl Pts',(0.346410161513776,0.489393102292058,0.2));
#9707=CARTESIAN_POINT('Ctrl Pts',(0.23094010767585,0.422726435625391,0.4));
#9708=CARTESIAN_POINT('',(0.23094010767585,0.422726435625391,-0.4));
#9709=CARTESIAN_POINT('Ctrl Pts',(0.23094010767585,0.422726435625391,-0.4));
#9710=CARTESIAN_POINT('Ctrl Pts',(0.346410161513775,0.489393102292058,-0.2));
#9711=CARTESIAN_POINT('Ctrl Pts',(0.461880215351701,0.422726435625391,0.));
#9712=CARTESIAN_POINT('',(-0.23094010767585,0.422726435625391,-0.4));
#9713=CARTESIAN_POINT('Ctrl Pts',(-0.23094010767585,0.422726435625391,-0.4));
#9714=CARTESIAN_POINT('Ctrl Pts',(-5.55111512312578E-17,0.489393102292058,
-0.4));
#9715=CARTESIAN_POINT('Ctrl Pts',(0.23094010767585,0.422726435625391,-0.4));
#9716=CARTESIAN_POINT('Ctrl Pts',(-0.461880215351701,0.422726435625391,
-5.6564012731995E-17));
#9717=CARTESIAN_POINT('Ctrl Pts',(-0.346410161513776,0.489393102292058,
-0.2));
#9718=CARTESIAN_POINT('Ctrl Pts',(-0.23094010767585,0.422726435625391,-0.4));
#9719=CARTESIAN_POINT('Origin',(0.23094010767585,0.,-0.4));
#9720=CARTESIAN_POINT('',(-0.23094010767585,0.,-0.4));
#9721=CARTESIAN_POINT('',(0.23094010767585,0.,-0.4));
#9722=CARTESIAN_POINT('Origin',(-0.23094010767585,0.,-0.4));
#9723=CARTESIAN_POINT('',(-0.461880215351701,0.,-5.6564012731995E-17));
#9724=CARTESIAN_POINT('Origin',(-0.461880215351701,0.,-5.6564012731995E-17));
#9725=CARTESIAN_POINT('',(-0.230940107675851,0.,0.4));
#9726=CARTESIAN_POINT('Origin',(0.,0.,0.));
#9727=CARTESIAN_POINT('',(-0.2117,0.47,2.59257727379495E-17));
#9728=CARTESIAN_POINT('Origin',(0.,0.47,0.));
#9729=CARTESIAN_POINT('',(-0.2117,0.,2.59257727379495E-17));
#9730=CARTESIAN_POINT('',(-0.2117,0.,2.59257727379495E-17));
#9731=CARTESIAN_POINT('Origin',(0.,0.,0.));
#9732=CARTESIAN_POINT('Origin',(-0.230940107675851,0.,0.4));
#9733=CARTESIAN_POINT('',(0.23094010767585,0.,0.4));
#9734=CARTESIAN_POINT('Origin',(0.461880215351701,0.,0.));
#9735=CARTESIAN_POINT('',(0.461880215351701,0.,0.));
#9736=CARTESIAN_POINT('Origin',(0.23094010767585,0.,0.4));
#9737=CARTESIAN_POINT('Origin',(0.,0.47,0.));
#9738=CARTESIAN_POINT('Origin',(0.,0.,0.));
#10469=UNCERTAINTY_MEASURE_WITH_UNIT(LENGTH_MEASURE(0.001),#10518,
'DISTANCE_ACCURACY_VALUE',
'Maximum model space distance between geometric entities at asserted c
onnectivities');
#10484=UNCERTAINTY_MEASURE_WITH_UNIT(LENGTH_MEASURE(0.001),#10518,
'DISTANCE_ACCURACY_VALUE',
'Maximum model space distance between geometric entities at asserted c
onnectivities');
#10502=(
GEOMETRIC_REPRESENTATION_CONTEXT(3)
GLOBAL_UNCERTAINTY_ASSIGNED_CONTEXT((#10469))
GLOBAL_UNIT_ASSIGNED_CONTEXT((#10518,#10520,#10521))
REPRESENTATION_CONTEXT('','3D')
);
#10517=(
GEOMETRIC_REPRESENTATION_CONTEXT(3)
GLOBAL_UNCERTAINTY_ASSIGNED_CONTEXT((#10484))
GLOBAL_UNIT_ASSIGNED_CONTEXT((#10518,#10520,#10521))
REPRESENTATION_CONTEXT('','3D')
);
#10518=(
LENGTH_UNIT()
NAMED_UNIT(*)
SI_UNIT(.CENTI.,.METRE.)
);
#10520=(
NAMED_UNIT(*)
PLANE_ANGLE_UNIT()
SI_UNIT($,.RADIAN.)
);
#10521=(
NAMED_UNIT(*)
SI_UNIT($,.STERADIAN.)
SOLID_ANGLE_UNIT()
);
#10539=SHAPE_DEFINITION_REPRESENTATION(#10571,#10658);
#10571=PRODUCT_DEFINITION_SHAPE('',$,#10691);
#10658=SHAPE_REPRESENTATION('',(#6604),#10502);
#10673=PRODUCT_DEFINITION_CONTEXT('part definition',#10771,'design');
#10691=PRODUCT_DEFINITION('Hex Nut - M5','Hex Nut - M5',#10723,#10673);
#10723=PRODUCT_DEFINITION_FORMATION('',$,#10790);
#10771=APPLICATION_CONTEXT(
'Core Data for Automotive Mechanical Design Process');
#10772=PRODUCT_CONTEXT('part definition',#10771,'mechanical');
#10790=PRODUCT('Hex Nut - M5','Hex Nut - M5','Hex Nut - M5',(#10772));
#10875=COLOUR_RGB('Black',0.12,0.14,0.17);
#10876=FILL_AREA_STYLE_COLOUR('',#10875);
#10877=FILL_AREA_STYLE('',(#10876));
#10878=SURFACE_STYLE_FILL_AREA(#10877);
#10879=SURFACE_SIDE_STYLE('',(#10878));
#10880=SURFACE_STYLE_USAGE(.BOTH.,#10879);
#10881=PRESENTATION_STYLE_ASSIGNMENT((#10880));
ENDSEC;
END-ISO-10303-21;
